ISO-10303-21;
HEADER;
/* Generated by software containing ST-Developer
 * from STEP Tools, Inc. (www.steptools.com) 
 */

FILE_DESCRIPTION(
/* description */ ('Flywheel Crank-Slider'),
/* implementation_level */ '2;1');

FILE_NAME(
/* name */ 'Flat Washer - M8.step',
/* time_stamp */ '2026-10-28T03:23:13-07:00',
/* author */ (''),
/* organization */ (''),
/* preprocessor_version */ 'ST-DEVELOPER v20.2',
/* originating_system */ 'Autodesk Translation Framework v15.17.0.0',
/* authorisation */ '');

FILE_SCHEMA (('AUTOMOTIVE_DESIGN { 1 0 10303 214 3 1 1 }'));
ENDSEC;

DATA;
#10=MECHANICAL_DESIGN_GEOMETRIC_PRESENTATION_REPRESENTATION('',(#683),#17322);
#578=SHAPE_REPRESENTATION_RELATIONSHIP('SRR','None',#17575,#630);
#630=ADVANCED_BREP_SHAPE_REPRESENTATION('',(#743),#17279);
#683=STYLED_ITEM('',(#17938),#743);
#743=MANIFOLD_SOLID_BREP('Body1',#9062);
#891=FACE_BOUND('',#2154,.T.);
#892=FACE_BOUND('',#2156,.T.);
#1120=PLANE('',#10051);
#1121=PLANE('',#10052);
#1510=FACE_OUTER_BOUND('',#2151,.T.);
#1511=FACE_OUTER_BOUND('',#2152,.T.);
#1512=FACE_OUTER_BOUND('',#2153,.T.);
#1513=FACE_OUTER_BOUND('',#2155,.T.);
#2151=EDGE_LOOP('',(#6930,#6931,#6932,#6933));
#2152=EDGE_LOOP('',(#6934,#6935,#6936,#6937));
#2153=EDGE_LOOP('',(#6938));
#2154=EDGE_LOOP('',(#6939));
#2155=EDGE_LOOP('',(#6940));
#2156=EDGE_LOOP('',(#6941));
#2846=LINE('',#15027,#3457);
#2847=LINE('',#15033,#3458);
#3457=VECTOR('',#11784,0.42);
#3458=VECTOR('',#11791,0.8);
#3988=CIRCLE('',#10046,0.42);
#3989=CIRCLE('',#10047,0.42);
#3990=CIRCLE('',#10049,0.8);
#3991=CIRCLE('',#10050,0.8);
#4547=VERTEX_POINT('',#15024);
#4548=VERTEX_POINT('',#15026);
#4549=VERTEX_POINT('',#15030);
#4550=VERTEX_POINT('',#15032);
#5422=EDGE_CURVE('',#4547,#4547,#3988,.T.);
#5423=EDGE_CURVE('',#4547,#4548,#2846,.T.);
#5424=EDGE_CURVE('',#4548,#4548,#3989,.T.);
#5425=EDGE_CURVE('',#4549,#4549,#3990,.T.);
#5426=EDGE_CURVE('',#4549,#4550,#2847,.T.);
#5427=EDGE_CURVE('',#4550,#4550,#3991,.T.);
#6930=ORIENTED_EDGE('',*,*,#5422,.F.);
#6931=ORIENTED_EDGE('',*,*,#5423,.T.);
#6932=ORIENTED_EDGE('',*,*,#5424,.T.);
#6933=ORIENTED_EDGE('',*,*,#5423,.F.);
#6934=ORIENTED_EDGE('',*,*,#5425,.F.);
#6935=ORIENTED_EDGE('',*,*,#5426,.T.);
#6936=ORIENTED_EDGE('',*,*,#5427,.T.);
#6937=ORIENTED_EDGE('',*,*,#5426,.F.);
#6938=ORIENTED_EDGE('',*,*,#5425,.T.);
#6939=ORIENTED_EDGE('',*,*,#5422,.T.);
#6940=ORIENTED_EDGE('',*,*,#5427,.F.);
#6941=ORIENTED_EDGE('',*,*,#5424,.F.);
#8405=CYLINDRICAL_SURFACE('',#10045,0.42);
#8406=CYLINDRICAL_SURFACE('',#10048,0.8);
#8701=ADVANCED_FACE('',(#1510),#8405,.F.);
#8702=ADVANCED_FACE('',(#1511),#8406,.T.);
#8703=ADVANCED_FACE('',(#1512,#891),#1120,.T.);
#8704=ADVANCED_FACE('',(#1513,#892),#1121,.F.);
#9062=CLOSED_SHELL('',(#8701,#8702,#8703,#8704));
#10044=AXIS2_PLACEMENT_3D('',#15022,#11778,#11779);
#10045=AXIS2_PLACEMENT_3D('',#15023,#11780,#11781);
#10046=AXIS2_PLACEMENT_3D('',#15025,#11782,#11783);
#10047=AXIS2_PLACEMENT_3D('',#15028,#11785,#11786);
#10048=AXIS2_PLACEMENT_3D('',#15029,#11787,#11788);
#10049=AXIS2_PLACEMENT_3D('',#15031,#11789,#11790);
#10050=AXIS2_PLACEMENT_3D('',#15034,#11792,#11793);
#10051=AXIS2_PLACEMENT_3D('',#15035,#11794,#11795);
#10052=AXIS2_PLACEMENT_3D('',#15036,#11796,#11797);
#11778=DIRECTION('axis',(0.,0.,1.));
#11779=DIRECTION('refdir',(1.,0.,0.));
#11780=DIRECTION('center_axis',(0.,1.,0.));
#11781=DIRECTION('ref_axis',(1.,0.,0.));
#11782=DIRECTION('center_axis',(0.,-1.,0.));
#11783=DIRECTION('ref_axis',(1.,0.,0.));
#11784=DIRECTION('',(0.,-1.,0.));
#11785=DIRECTION('center_axis',(0.,-1.,0.));
#11786=DIRECTION('ref_axis',(1.,0.,0.));
#11787=DIRECTION('center_axis',(0.,1.,0.));
#11788=DIRECTION('ref_axis',(1.,0.,0.));
#11789=DIRECTION('center_axis',(0.,1.,0.));
#11790=DIRECTION('ref_axis',(1.,0.,0.));
#11791=DIRECTION('',(0.,-1.,0.));
#11792=DIRECTION('center_axis',(0.,1.,0.));
#11793=DIRECTION('ref_axis',(1.,0.,0.));
#11794=DIRECTION('center_axis',(0.,1.,0.));
#11795=DIRECTION('ref_axis',(1.,0.,0.));
#11796=DIRECTION('center_axis',(0.,1.,0.));
#11797=DIRECTION('ref_axis',(1.,0.,0.));
#15022=CARTESIAN_POINT('',(0.,0.,0.));
#15023=CARTESIAN_POINT('Origin',(0.,0.,0.));
#15024=CARTESIAN_POINT('',(-0.42,0.16,5.14351655641888E-17));
#15025=CARTESIAN_POINT('Origin',(0.,0.16,0.));
#15026=CARTESIAN_POINT('',(-0.42,0.,5.14351655641888E-17));
#15027=CARTESIAN_POINT('',(-0.42,0.,5.14351655641888E-17));
#15028=CARTESIAN_POINT('Origin',(0.,0.,0.));
#15029=CARTESIAN_POINT('Origin',(0.,0.,0.));
#15030=CARTESIAN_POINT('',(-0.8,0.16,9.79717439317883E-17));
#15031=CARTESIAN_POINT('Origin',(0.,0.16,0.));
#15032=CARTESIAN_POINT('',(-0.8,0.,9.79717439317883E-17));
#15033=CARTESIAN_POINT('',(-0.8,0.,9.79717439317883E-17));
#15034=CARTESIAN_POINT('Origin',(0.,0.,0.));
#15035=CARTESIAN_POINT('Origin',(0.,0.16,0.));
#15036=CARTESIAN_POINT('Origin',(0.,0.,0.));
#17218=UNCERTAINTY_MEASURE_WITH_UNIT(LENGTH_MEASURE(0.001),#17323,
'DISTANCE_ACCURACY_VALUE',
'Maximum model space distance between geometric entities at asserted c
onnectivities');
#17261=UNCERTAINTY_MEASURE_WITH_UNIT(LENGTH_MEASURE(0.001),#17323,
'DISTANCE_ACCURACY_VALUE',
'Maximum model space distance between geometric entities at asserted c
onnectivities');
#17279=(
GEOMETRIC_REPRESENTATION_CONTEXT(3)
GLOBAL_UNCERTAINTY_ASSIGNED_CONTEXT((#17218))
GLOBAL_UNIT_ASSIGNED_CONTEXT((#17323,#17325,#17326))
REPRESENTATION_CONTEXT('','3D')
);
#17322=(
GEOMETRIC_REPRESENTATION_CONTEXT(3)
GLOBAL_UNCERTAINTY_ASSIGNED_CONTEXT((#17261))
GLOBAL_UNIT_ASSIGNED_CONTEXT((#17323,#17325,#17326))
REPRESENTATION_CONTEXT('','3D')
);
#17323=(
LENGTH_UNIT()
NAMED_UNIT(*)
SI_UNIT(.CENTI.,.METRE.)
);
#17325=(
NAMED_UNIT(*)
PLANE_ANGLE_UNIT()
SI_UNIT($,.RADIAN.)
);
#17326=(
NAMED_UNIT(*)
SI_UNIT($,.STERADIAN.)
SOLID_ANGLE_UNIT()
);
#17344=SHAPE_DEFINITION_REPRESENTATION(#17406,#17575);
#17406=PRODUCT_DEFINITION_SHAPE('',$,#17636);
#17575=SHAPE_REPRESENTATION('',(#10044),#17279);
#17618=PRODUCT_DEFINITION_CONTEXT('part definition',#17800,'design');
#17636=PRODUCT_DEFINITION('Flat Washer - M8','Flat Washer - M8',#17696,
#17618);
#17696=PRODUCT_DEFINITION_FORMATION('',$,#17819);
#17800=APPLICATION_CONTEXT(
'Core Data for Automotive Mechanical Design Process');
#17801=PRODUCT_CONTEXT('part definition',#17800,'mechanical');
#17819=PRODUCT('Flat Washer - M8','Flat Washer - M8','Flat Washer - M8',
(#17801));
#17932=COLOUR_RGB('Black',0.12,0.14,0.17);
#17933=FILL_AREA_STYLE_COLOUR('',#17932);
#17934=FILL_AREA_STYLE('',(#17933));
#17935=SURFACE_STYLE_FILL_AREA(#17934);
#17936=SURFACE_SIDE_STYLE('',(#17935));
#17937=SURFACE_STYLE_USAGE(.BOTH.,#17936);
#17938=PRESENTATION_STYLE_ASSIGNMENT((#17937));
ENDSEC;
END-ISO-10303-21;
